ISO-10303-21;
HEADER;
/* Generated by software containing ST-Developer
 * from STEP Tools, Inc. (www.steptools.com) 
 */

FILE_DESCRIPTION(
/* description */ ('Turntable on roller ring'),
/* implementation_level */ '2;1');

FILE_NAME(
/* name */ 'Inner race spacer (4).step',
/* time_stamp */ '2026-10-28T03:23:59-07:00',
/* author */ (''),
/* organization */ (''),
/* preprocessor_version */ 'ST-DEVELOPER v20.2',
/* originating_system */ 'Autodesk Translation Framework v15.17.0.0',
/* authorisation */ '');

FILE_SCHEMA (('AUTOMOTIVE_DESIGN { 1 0 10303 214 3 1 1 }'));
ENDSEC;

DATA;
#10=MECHANICAL_DESIGN_GEOMETRIC_PRESENTATION_REPRESENTATION('',(#654),#16281);
#535=SHAPE_REPRESENTATION_RELATIONSHIP('SRR','None',#16554,#590);
#590=ADVANCED_BREP_SHAPE_REPRESENTATION('',(#724),#16248);
#654=STYLED_ITEM('',(#16932),#724);
#724=MANIFOLD_SOLID_BREP('Body1',#8397);
#927=FACE_BOUND('',#2249,.T.);
#928=FACE_BOUND('',#2251,.T.);
#1155=PLANE('',#9743);
#1156=PLANE('',#9744);
#1571=FACE_OUTER_BOUND('',#2246,.T.);
#1572=FACE_OUTER_BOUND('',#2247,.T.);
#1573=FACE_OUTER_BOUND('',#2248,.T.);
#1574=FACE_OUTER_BOUND('',#2250,.T.);
#2246=EDGE_LOOP('',(#6995,#6996,#6997,#6998));
#2247=EDGE_LOOP('',(#6999,#7000,#7001,#7002));
#2248=EDGE_LOOP('',(#7003));
#2249=EDGE_LOOP('',(#7004));
#2250=EDGE_LOOP('',(#7005));
#2251=EDGE_LOOP('',(#7006));
#2833=LINE('',#14954,#3316);
#2834=LINE('',#14960,#3317);
#3316=VECTOR('',#11938,0.505);
#3317=VECTOR('',#11945,0.7);
#3773=CIRCLE('',#9738,0.505);
#3774=CIRCLE('',#9739,0.505);
#3775=CIRCLE('',#9741,0.7);
#3776=CIRCLE('',#9742,0.7);
#4401=VERTEX_POINT('',#14951);
#4402=VERTEX_POINT('',#14953);
#4403=VERTEX_POINT('',#14957);
#4404=VERTEX_POINT('',#14959);
#5308=EDGE_CURVE('',#4401,#4401,#3773,.T.);
#5309=EDGE_CURVE('',#4401,#4402,#2833,.T.);
#5310=EDGE_CURVE('',#4402,#4402,#3774,.T.);
#5311=EDGE_CURVE('',#4403,#4403,#3775,.T.);
#5312=EDGE_CURVE('',#4403,#4404,#2834,.T.);
#5313=EDGE_CURVE('',#4404,#4404,#3776,.T.);
#6995=ORIENTED_EDGE('',*,*,#5308,.F.);
#6996=ORIENTED_EDGE('',*,*,#5309,.T.);
#6997=ORIENTED_EDGE('',*,*,#5310,.T.);
#6998=ORIENTED_EDGE('',*,*,#5309,.F.);
#6999=ORIENTED_EDGE('',*,*,#5311,.F.);
#7000=ORIENTED_EDGE('',*,*,#5312,.T.);
#7001=ORIENTED_EDGE('',*,*,#5313,.T.);
#7002=ORIENTED_EDGE('',*,*,#5312,.F.);
#7003=ORIENTED_EDGE('',*,*,#5311,.T.);
#7004=ORIENTED_EDGE('',*,*,#5308,.T.);
#7005=ORIENTED_EDGE('',*,*,#5313,.F.);
#7006=ORIENTED_EDGE('',*,*,#5310,.F.);
#7792=CYLINDRICAL_SURFACE('',#9737,0.505);
#7793=CYLINDRICAL_SURFACE('',#9740,0.7);
#8174=ADVANCED_FACE('',(#1571),#7792,.F.);
#8175=ADVANCED_FACE('',(#1572),#7793,.T.);
#8176=ADVANCED_FACE('',(#1573,#927),#1155,.T.);
#8177=ADVANCED_FACE('',(#1574,#928),#1156,.F.);
#8397=CLOSED_SHELL('',(#8174,#8175,#8176,#8177));
#9736=AXIS2_PLACEMENT_3D('',#14949,#11932,#11933);
#9737=AXIS2_PLACEMENT_3D('',#14950,#11934,#11935);
#9738=AXIS2_PLACEMENT_3D('',#14952,#11936,#11937);
#9739=AXIS2_PLACEMENT_3D('',#14955,#11939,#11940);
#9740=AXIS2_PLACEMENT_3D('',#14956,#11941,#11942);
#9741=AXIS2_PLACEMENT_3D('',#14958,#11943,#11944);
#9742=AXIS2_PLACEMENT_3D('',#14961,#11946,#11947);
#9743=AXIS2_PLACEMENT_3D('',#14962,#11948,#11949);
#9744=AXIS2_PLACEMENT_3D('',#14963,#11950,#11951);
#11932=DIRECTION('axis',(0.,0.,1.));
#11933=DIRECTION('refdir',(1.,0.,0.));
#11934=DIRECTION('center_axis',(0.,1.,0.));
#11935=DIRECTION('ref_axis',(1.,0.,0.));
#11936=DIRECTION('center_axis',(0.,-1.,0.));
#11937=DIRECTION('ref_axis',(1.,0.,0.));
#11938=DIRECTION('',(0.,-1.,0.));
#11939=DIRECTION('center_axis',(0.,-1.,0.));
#11940=DIRECTION('ref_axis',(1.,0.,0.));
#11941=DIRECTION('center_axis',(0.,1.,0.));
#11942=DIRECTION('ref_axis',(1.,0.,0.));
#11943=DIRECTION('center_axis',(0.,1.,0.));
#11944=DIRECTION('ref_axis',(1.,0.,0.));
#11945=DIRECTION('',(0.,-1.,0.));
#11946=DIRECTION('center_axis',(0.,1.,0.));
#11947=DIRECTION('ref_axis',(1.,0.,0.));
#11948=DIRECTION('center_axis',(0.,1.,0.));
#11949=DIRECTION('ref_axis',(1.,0.,0.));
#11950=DIRECTION('center_axis',(0.,1.,0.));
#11951=DIRECTION('ref_axis',(1.,0.,0.));
#14949=CARTESIAN_POINT('',(0.,0.,0.));
#14950=CARTESIAN_POINT('Origin',(0.,14.1,3.5));
#14951=CARTESIAN_POINT('',(-0.505,14.55,3.5));
#14952=CARTESIAN_POINT('Origin',(0.,14.55,3.5));
#14953=CARTESIAN_POINT('',(-0.505,14.1,3.5));
#14954=CARTESIAN_POINT('',(-0.505,14.1,3.5));
#14955=CARTESIAN_POINT('Origin',(0.,14.1,3.5));
#14956=CARTESIAN_POINT('Origin',(0.,14.1,3.5));
#14957=CARTESIAN_POINT('',(-0.7,14.55,3.5));
#14958=CARTESIAN_POINT('Origin',(0.,14.55,3.5));
#14959=CARTESIAN_POINT('',(-0.7,14.1,3.5));
#14960=CARTESIAN_POINT('',(-0.7,14.1,3.5));
#14961=CARTESIAN_POINT('Origin',(0.,14.1,3.5));
#14962=CARTESIAN_POINT('Origin',(0.,14.55,3.5));
#14963=CARTESIAN_POINT('Origin',(0.,14.1,3.5));
#16179=UNCERTAINTY_MEASURE_WITH_UNIT(LENGTH_MEASURE(0.001),#16282,
'DISTANCE_ACCURACY_VALUE',
'Maximum model space distance between geometric entities at asserted c
onnectivities');
#16212=UNCERTAINTY_MEASURE_WITH_UNIT(LENGTH_MEASURE(0.001),#16282,
'DISTANCE_ACCURACY_VALUE',
'Maximum model space distance between geometric entities at asserted c
onnectivities');
#16248=(
GEOMETRIC_REPRESENTATION_CONTEXT(3)
GLOBAL_UNCERTAINTY_ASSIGNED_CONTEXT((#16179))
GLOBAL_UNIT_ASSIGNED_CONTEXT((#16282,#16284,#16285))
REPRESENTATION_CONTEXT('','3D')
);
#16281=(
GEOMETRIC_REPRESENTATION_CONTEXT(3)
GLOBAL_UNCERTAINTY_ASSIGNED_CONTEXT((#16212))
GLOBAL_UNIT_ASSIGNED_CONTEXT((#16282,#16284,#16285))
REPRESENTATION_CONTEXT('','3D')
);
#16282=(
LENGTH_UNIT()
NAMED_UNIT(*)
SI_UNIT(.CENTI.,.METRE.)
);
#16284=(
NAMED_UNIT(*)
PLANE_ANGLE_UNIT()
SI_UNIT($,.RADIAN.)
);
#16285=(
NAMED_UNIT(*)
SI_UNIT($,.STERADIAN.)
SOLID_ANGLE_UNIT()
);
#16321=SHAPE_DEFINITION_REPRESENTATION(#16415,#16554);
#16415=PRODUCT_DEFINITION_SHAPE('',$,#16623);
#16554=SHAPE_REPRESENTATION('',(#9736),#16248);
#16587=PRODUCT_DEFINITION_CONTEXT('part definition',#16793,'design');
#16623=PRODUCT_DEFINITION('Inner race spacer (4)','Inner race spacer (4)',
#16691,#16587);
#16691=PRODUCT_DEFINITION_FORMATION('',$,#16830);
#16793=APPLICATION_CONTEXT(
'Core Data for Automotive Mechanical Design Process');
#16794=PRODUCT_CONTEXT('part definition',#16793,'mechanical');
#16830=PRODUCT('Inner race spacer (4)','Inner race spacer (4)',
'Inner race spacer (4)',(#16794));
#16926=COLOUR_RGB('Grey',0.48,0.52,0.57);
#16927=FILL_AREA_STYLE_COLOUR('',#16926);
#16928=FILL_AREA_STYLE('',(#16927));
#16929=SURFACE_STYLE_FILL_AREA(#16928);
#16930=SURFACE_SIDE_STYLE('',(#16929));
#16931=SURFACE_STYLE_USAGE(.BOTH.,#16930);
#16932=PRESENTATION_STYLE_ASSIGNMENT((#16931));
ENDSEC;
END-ISO-10303-21;
